ISO-10303-21;
HEADER;
/* Generated by software containing ST-Developer
 * from STEP Tools, Inc. (www.steptools.com) 
 */

FILE_DESCRIPTION(
/* description */ ('PAT-099'),
/* implementation_level */ '2;1');

FILE_NAME(
/* name */ 'Roller inner-race spacer (1).step',
/* time_stamp */ '2026-10-29T17:25:42-07:00',
/* author */ (''),
/* organization */ (''),
/* preprocessor_version */ 'ST-DEVELOPER v20.2',
/* originating_system */ 'Autodesk Translation Framework v15.17.0.0',
/* authorisation */ '');

FILE_SCHEMA (('AUTOMOTIVE_DESIGN { 1 0 10303 214 3 1 1 }'));
ENDSEC;

DATA;
#10=MECHANICAL_DESIGN_GEOMETRIC_PRESENTATION_REPRESENTATION('',(#354),#11035);
#304=SHAPE_REPRESENTATION_RELATIONSHIP('SRR','None',#11175,#329);
#329=ADVANCED_BREP_SHAPE_REPRESENTATION('',(#386),#11025);
#354=STYLED_ITEM('',(#11379),#386);
#386=MANIFOLD_SOLID_BREP('Body1',#4723);
#509=FACE_BOUND('',#1257,.T.);
#510=FACE_BOUND('',#1259,.T.);
#627=PLANE('',#5460);
#628=PLANE('',#5461);
#865=FACE_OUTER_BOUND('',#1254,.T.);
#866=FACE_OUTER_BOUND('',#1255,.T.);
#867=FACE_OUTER_BOUND('',#1256,.T.);
#868=FACE_OUTER_BOUND('',#1258,.T.);
#1254=EDGE_LOOP('',(#4013,#4014,#4015,#4016));
#1255=EDGE_LOOP('',(#4017,#4018,#4019,#4020));
#1256=EDGE_LOOP('',(#4021));
#1257=EDGE_LOOP('',(#4022));
#1258=EDGE_LOOP('',(#4023));
#1259=EDGE_LOOP('',(#4024));
#1552=LINE('',#10254,#1804);
#1553=LINE('',#10260,#1805);
#1804=VECTOR('',#6757,0.505);
#1805=VECTOR('',#6764,0.7);
#2051=CIRCLE('',#5455,0.505);
#2052=CIRCLE('',#5456,0.505);
#2053=CIRCLE('',#5458,0.7);
#2054=CIRCLE('',#5459,0.7);
#2435=VERTEX_POINT('',#10251);
#2436=VERTEX_POINT('',#10253);
#2437=VERTEX_POINT('',#10257);
#2438=VERTEX_POINT('',#10259);
#2983=EDGE_CURVE('',#2435,#2435,#2051,.T.);
#2984=EDGE_CURVE('',#2435,#2436,#1552,.T.);
#2985=EDGE_CURVE('',#2436,#2436,#2052,.T.);
#2986=EDGE_CURVE('',#2437,#2437,#2053,.T.);
#2987=EDGE_CURVE('',#2437,#2438,#1553,.T.);
#2988=EDGE_CURVE('',#2438,#2438,#2054,.T.);
#4013=ORIENTED_EDGE('',*,*,#2983,.F.);
#4014=ORIENTED_EDGE('',*,*,#2984,.T.);
#4015=ORIENTED_EDGE('',*,*,#2985,.T.);
#4016=ORIENTED_EDGE('',*,*,#2984,.F.);
#4017=ORIENTED_EDGE('',*,*,#2986,.F.);
#4018=ORIENTED_EDGE('',*,*,#2987,.T.);
#4019=ORIENTED_EDGE('',*,*,#2988,.T.);
#4020=ORIENTED_EDGE('',*,*,#2987,.F.);
#4021=ORIENTED_EDGE('',*,*,#2986,.T.);
#4022=ORIENTED_EDGE('',*,*,#2983,.T.);
#4023=ORIENTED_EDGE('',*,*,#2988,.F.);
#4024=ORIENTED_EDGE('',*,*,#2985,.F.);
#4406=CYLINDRICAL_SURFACE('',#5454,0.505);
#4407=CYLINDRICAL_SURFACE('',#5457,0.7);
#4630=ADVANCED_FACE('',(#865),#4406,.F.);
#4631=ADVANCED_FACE('',(#866),#4407,.T.);
#4632=ADVANCED_FACE('',(#867,#509),#627,.T.);
#4633=ADVANCED_FACE('',(#868,#510),#628,.F.);
#4723=CLOSED_SHELL('',(#4630,#4631,#4632,#4633));
#5453=AXIS2_PLACEMENT_3D('',#10249,#6751,#6752);
#5454=AXIS2_PLACEMENT_3D('',#10250,#6753,#6754);
#5455=AXIS2_PLACEMENT_3D('',#10252,#6755,#6756);
#5456=AXIS2_PLACEMENT_3D('',#10255,#6758,#6759);
#5457=AXIS2_PLACEMENT_3D('',#10256,#6760,#6761);
#5458=AXIS2_PLACEMENT_3D('',#10258,#6762,#6763);
#5459=AXIS2_PLACEMENT_3D('',#10261,#6765,#6766);
#5460=AXIS2_PLACEMENT_3D('',#10262,#6767,#6768);
#5461=AXIS2_PLACEMENT_3D('',#10263,#6769,#6770);
#6751=DIRECTION('axis',(0.,0.,1.));
#6752=DIRECTION('refdir',(1.,0.,0.));
#6753=DIRECTION('center_axis',(0.,0.,1.));
#6754=DIRECTION('ref_axis',(1.,0.,0.));
#6755=DIRECTION('center_axis',(0.,0.,-1.));
#6756=DIRECTION('ref_axis',(1.,0.,0.));
#6757=DIRECTION('',(0.,0.,-1.));
#6758=DIRECTION('center_axis',(0.,0.,-1.));
#6759=DIRECTION('ref_axis',(1.,0.,0.));
#6760=DIRECTION('center_axis',(0.,0.,1.));
#6761=DIRECTION('ref_axis',(1.,0.,0.));
#6762=DIRECTION('center_axis',(0.,0.,1.));
#6763=DIRECTION('ref_axis',(1.,0.,0.));
#6764=DIRECTION('',(0.,0.,-1.));
#6765=DIRECTION('center_axis',(0.,0.,1.));
#6766=DIRECTION('ref_axis',(1.,0.,0.));
#6767=DIRECTION('center_axis',(0.,0.,1.));
#6768=DIRECTION('ref_axis',(1.,0.,0.));
#6769=DIRECTION('center_axis',(0.,0.,1.));
#6770=DIRECTION('ref_axis',(1.,0.,0.));
#10249=CARTESIAN_POINT('',(0.,0.,0.));
#10250=CARTESIAN_POINT('Origin',(4.,0.,5.7));
#10251=CARTESIAN_POINT('',(3.495,-6.18446633569413E-17,5.9));
#10252=CARTESIAN_POINT('Origin',(4.,0.,5.9));
#10253=CARTESIAN_POINT('',(3.495,-6.18446633569413E-17,5.7));
#10254=CARTESIAN_POINT('',(3.495,-6.18446633569413E-17,5.7));
#10255=CARTESIAN_POINT('Origin',(4.,0.,5.7));
#10256=CARTESIAN_POINT('Origin',(4.,0.,5.7));
#10257=CARTESIAN_POINT('',(3.3,-8.57252759403147E-17,5.9));
#10258=CARTESIAN_POINT('Origin',(4.,0.,5.9));
#10259=CARTESIAN_POINT('',(3.3,-8.57252759403147E-17,5.7));
#10260=CARTESIAN_POINT('',(3.3,-8.57252759403147E-17,5.7));
#10261=CARTESIAN_POINT('Origin',(4.,0.,5.7));
#10262=CARTESIAN_POINT('Origin',(4.,0.,5.9));
#10263=CARTESIAN_POINT('Origin',(4.,0.,5.7));
#10992=UNCERTAINTY_MEASURE_WITH_UNIT(LENGTH_MEASURE(0.001),#11036,
'DISTANCE_ACCURACY_VALUE',
'Maximum model space distance between geometric entities at asserted c
onnectivities');
#11002=UNCERTAINTY_MEASURE_WITH_UNIT(LENGTH_MEASURE(0.001),#11036,
'DISTANCE_ACCURACY_VALUE',
'Maximum model space distance between geometric entities at asserted c
onnectivities');
#11025=(
GEOMETRIC_REPRESENTATION_CONTEXT(3)
GLOBAL_UNCERTAINTY_ASSIGNED_CONTEXT((#10992))
GLOBAL_UNIT_ASSIGNED_CONTEXT((#11036,#11038,#11039))
REPRESENTATION_CONTEXT('','3D')
);
#11035=(
GEOMETRIC_REPRESENTATION_CONTEXT(3)
GLOBAL_UNCERTAINTY_ASSIGNED_CONTEXT((#11002))
GLOBAL_UNIT_ASSIGNED_CONTEXT((#11036,#11038,#11039))
REPRESENTATION_CONTEXT('','3D')
);
#11036=(
LENGTH_UNIT()
NAMED_UNIT(*)
SI_UNIT(.CENTI.,.METRE.)
);
#11038=(
NAMED_UNIT(*)
PLANE_ANGLE_UNIT()
SI_UNIT($,.RADIAN.)
);
#11039=(
NAMED_UNIT(*)
SI_UNIT($,.STERADIAN.)
SOLID_ANGLE_UNIT()
);
#11062=SHAPE_DEFINITION_REPRESENTATION(#11100,#11175);
#11100=PRODUCT_DEFINITION_SHAPE('',$,#11208);
#11175=SHAPE_REPRESENTATION('',(#5453),#11025);
#11185=PRODUCT_DEFINITION_CONTEXT('part definition',#11283,'design');
#11208=PRODUCT_DEFINITION('Roller inner-race spacer (1)',
'Roller inner-race spacer (1)',#11240,#11185);
#11240=PRODUCT_DEFINITION_FORMATION('',$,#11307);
#11283=APPLICATION_CONTEXT(
'Core Data for Automotive Mechanical Design Process');
#11284=PRODUCT_CONTEXT('part definition',#11283,'mechanical');
#11307=PRODUCT('Roller inner-race spacer (1)',
'Roller inner-race spacer (1)','Roller inner-race spacer (1)',(#11284));
#11373=COLOUR_RGB('Sky Blue',0.24,0.69,0.87);
#11374=FILL_AREA_STYLE_COLOUR('',#11373);
#11375=FILL_AREA_STYLE('',(#11374));
#11376=SURFACE_STYLE_FILL_AREA(#11375);
#11377=SURFACE_SIDE_STYLE('',(#11376));
#11378=SURFACE_STYLE_USAGE(.BOTH.,#11377);
#11379=PRESENTATION_STYLE_ASSIGNMENT((#11378));
ENDSEC;
END-ISO-10303-21;
